ISO-10303-21;
HEADER;
FILE_DESCRIPTION (('STEP AP214'),
    '1' );
FILE_NAME ('vertical suport.step',
    '2026-10-24T13:33:06',
    ( '' ),
    ( '' ),
    'SwSTEP 2.0',
    'SolidWorks 2026',
    '' );
FILE_SCHEMA (( 'AUTOMOTIVE_DESIGN' ));
ENDSEC;

DATA;
#15=DIRECTION ( 'NONE',  ( -0.000000000000000000, -0.000000000000000000, -1.000000000000000000 ) ) ;
#16=EDGE_CURVE ( 'NONE', #12113, #10379, #13864, .T. ) ;
#24=CYLINDRICAL_SURFACE ( 'NONE', #7328, 2.649999999999985700 ) ;
#57=ORIENTED_EDGE ( 'NONE', *, *, #5179, .T. ) ;
#64=EDGE_CURVE ( 'NONE', #764, #13509, #648, .T. ) ;
#79=DIRECTION ( 'NONE',  ( 1.000000000000000000, 0.000000000000000000, 0.000000000000000000 ) ) ;
#87=CARTESIAN_POINT ( 'NONE',  ( 134.9999999999999432, -36.99999999999997868, 0.000000000000000000 ) ) ;
#159=STYLED_ITEM('',(#14424),#13163);
#270=AXIS2_PLACEMENT_3D ( 'NONE', #3591, #10188, #1328 ) ;
#316=CARTESIAN_POINT ( 'NONE',  ( 134.9999999999999432, -36.99999999999997868, 10.00000000000000000 ) ) ;
#648=LINE ( 'NONE', #5110, #4286 ) ;
#752=EDGE_LOOP ( 'NONE', ( #1446, #5802, #10975, #13060 ) ) ;
#764=VERTEX_POINT ( 'NONE', #2524 ) ;
#773=CARTESIAN_POINT ( 'NONE',  ( 124.9999999999999574, -64.99999999999997158, 10.00000000000000000 ) ) ;
#886=ADVANCED_FACE ( 'NONE', ( #1485 ), #8095, .F. ) ;
#909=AXIS2_PLACEMENT_3D ( 'NONE', #4923, #10280, #7233 ) ;
#1044=CARTESIAN_POINT ( 'NONE',  ( 124.9999999999999858, 55.00000000000000711, 10.00000000000000000 ) ) ;
#1111=VERTEX_POINT ( 'NONE', #9561 ) ;
#1256=DIRECTION ( 'NONE',  ( 0.000000000000000000, 0.000000000000000000, -1.000000000000000000 ) ) ;
#1324=FACE_OUTER_BOUND ( 'NONE', #13084, .T. ) ;
#1328=DIRECTION ( 'NONE',  ( 1.000000000000000000, 0.000000000000000000, 0.000000000000000000 ) ) ;
#1362=ORIENTED_EDGE ( 'NONE', *, *, #7124, .T. ) ;
#1394=CARTESIAN_POINT ( 'NONE',  ( 132.3499999999999659, -56.99999999999997158, 10.00000000000000000 ) ) ;
#1413=EDGE_CURVE ( 'NONE', #13509, #4208, #3762, .T. ) ;
#1436=CARTESIAN_POINT ( 'NONE',  ( 137.6499999999999488, -36.99999999999997868, 10.00000000000000178 ) ) ;
#1446=ORIENTED_EDGE ( 'NONE', *, *, #2292, .T. ) ;
#1471=PLANE ( 'NONE',  #12390 ) ;
#1477=ORIENTED_EDGE ( 'NONE', *, *, #2537, .T. ) ;
#1485=FACE_OUTER_BOUND ( 'NONE', #5885, .T. ) ;
#1542=CARTESIAN_POINT ( 'NONE',  ( 134.9999999999999432, -36.99999999999997868, 10.00000000000000000 ) ) ;
#1551=CIRCLE ( 'NONE', #6442, 2.649999999999985700 ) ;
#1613=EDGE_CURVE ( 'NONE', #13461, #8622, #8044, .T. ) ;
#1634=EDGE_LOOP ( 'NONE', ( #5750, #1743, #13000, #57 ) ) ;
#1709=DIRECTION ( 'NONE',  ( -1.000000000000000000, 2.312964634635743450E-16, 0.000000000000000000 ) ) ;
#1743=ORIENTED_EDGE ( 'NONE', *, *, #2065, .T. ) ;
#1771=VECTOR ( 'NONE', #2160, 1000.000000000000000 ) ;
#1817=SURFACE_STYLE_USAGE ( .BOTH. , #14141 ) ;
#1848=( LENGTH_UNIT ( ) NAMED_UNIT ( * ) SI_UNIT ( .MILLI., .METRE. ) );
#1857=DIRECTION ( 'NONE',  ( -1.000000000000000000, 0.000000000000000000, 0.000000000000000000 ) ) ;
#1919=CARTESIAN_POINT ( 'NONE',  ( 132.3499999999999943, 45.00000000000001421, 0.000000000000000000 ) ) ;
#1929=CARTESIAN_POINT ( 'NONE',  ( 134.9999999999999432, -36.99999999999997868, 0.000000000000000000 ) ) ;
#1971=VERTEX_POINT ( 'NONE', #11900 ) ;
#1988=VECTOR ( 'NONE', #8190, 1000.000000000000000 ) ;
#2065=EDGE_CURVE ( 'NONE', #3349, #6820, #11583, .T. ) ;
#2091=ORIENTED_EDGE ( 'NONE', *, *, #3400, .T. ) ;
#2128=CARTESIAN_POINT ( 'NONE',  ( 134.9999999999999432, -36.99999999999997868, 10.00000000000000178 ) ) ;
#2147=DIRECTION ( 'NONE',  ( -0.000000000000000000, -0.000000000000000000, 1.000000000000000000 ) ) ;
#2150=EDGE_CURVE ( 'NONE', #4208, #13509, #3942, .T. ) ;
#2160=DIRECTION ( 'NONE',  ( 2.312964634635743450E-16, 1.000000000000000000, 0.000000000000000000 ) ) ;
#2196=EDGE_CURVE ( 'NONE', #8622, #10379, #9772, .T. ) ;
#2202=ORIENTED_EDGE ( 'NONE', *, *, #8150, .T. ) ;
#2257=EDGE_LOOP ( 'NONE', ( #7508, #5212, #2594, #9324 ) ) ;
#2292=EDGE_CURVE ( 'NONE', #1971, #4138, #8213, .T. ) ;
#2333=ORIENTED_EDGE ( 'NONE', *, *, #4805, .T. ) ;
#2341=CARTESIAN_POINT ( 'NONE',  ( 134.9999999999999432, -56.99999999999997158, 10.00000000000000000 ) ) ;
#2359=DIRECTION ( 'NONE',  ( -1.000000000000000000, 0.000000000000000000, -0.000000000000000000 ) ) ;
#2360=EDGE_CURVE ( 'NONE', #3993, #5384, #5763, .T. ) ;
#2362=DIRECTION ( 'NONE',  ( 1.000000000000000000, 0.000000000000000000, 0.000000000000000000 ) ) ;
#2398=ADVANCED_FACE ( 'NONE', ( #11282, #6923, #6996, #11429 ), #1471, .F. ) ;
#2404=CARTESIAN_POINT ( 'NONE',  ( 134.9999999999999432, -56.99999999999997158, 0.000000000000000000 ) ) ;
#2427=ADVANCED_FACE ( 'NONE', ( #10190 ), #2508, .F. ) ;
#2508=CYLINDRICAL_SURFACE ( 'NONE', #7524, 2.649999999999985700 ) ;
#2524=CARTESIAN_POINT ( 'NONE',  ( 137.6499999999999773, 45.00000000000001421, 10.00000000000000000 ) ) ;
#2537=EDGE_CURVE ( 'NONE', #1111, #4205, #10637, .T. ) ;
#2545=AXIS2_PLACEMENT_3D ( 'NONE', #3756, #1709, #7299 ) ;
#2547=DIRECTION ( 'NONE',  ( -1.000000000000000000, 0.000000000000000000, 0.000000000000000000 ) ) ;
#2550=CARTESIAN_POINT ( 'NONE',  ( 124.9999999999999858, 55.00000000000000711, 10.00000000000000000 ) ) ;
#2573=FACE_OUTER_BOUND ( 'NONE', #9828, .T. ) ;
#2594=ORIENTED_EDGE ( 'NONE', *, *, #1613, .T. ) ;
#2698=AXIS2_PLACEMENT_3D ( 'NONE', #773, #5233, #7677 ) ;
#2774=ADVANCED_FACE ( 'NONE', ( #6391 ), #9734, .F. ) ;
#2881=EDGE_CURVE ( 'NONE', #764, #7188, #7370, .T. ) ;
#2906=AXIS2_PLACEMENT_3D ( 'NONE', #13308, #14109, #6503 ) ;
#2994=( NAMED_UNIT ( * ) PLANE_ANGLE_UNIT ( ) SI_UNIT ( $, .RADIAN. ) );
#3056=( GEOMETRIC_REPRESENTATION_CONTEXT ( 3 ) GLOBAL_UNCERTAINTY_ASSIGNED_CONTEXT ( ( #8848 ) ) GLOBAL_UNIT_ASSIGNED_CONTEXT ( ( #3641, #11616, #12775 ) ) REPRESENTATION_CONTEXT ( 'NONE', 'WORKASPACE' ) );
#3057=ORIENTED_EDGE ( 'NONE', *, *, #11462, .F. ) ;
#3058=DIRECTION ( 'NONE',  ( 1.000000000000000000, 0.000000000000000000, 0.000000000000000000 ) ) ;
#3097=( GEOMETRIC_REPRESENTATION_CONTEXT ( 3 ) GLOBAL_UNCERTAINTY_ASSIGNED_CONTEXT ( ( #6293 ) ) GLOBAL_UNIT_ASSIGNED_CONTEXT ( ( #4002, #2994, #11979 ) ) REPRESENTATION_CONTEXT ( 'NONE', 'WORKASPACE' ) );
#3184=DIRECTION ( 'NONE',  ( 2.312964634635743450E-16, 1.000000000000000000, 0.000000000000000000 ) ) ;
#3248=DIRECTION ( 'NONE',  ( -0.000000000000000000, -0.000000000000000000, -1.000000000000000000 ) ) ;
#3261=LINE ( 'NONE', #12099, #1771 ) ;
#3314=VECTOR ( 'NONE', #12269, 1000.000000000000000 ) ;
#3349=VERTEX_POINT ( 'NONE', #9984 ) ;
#3361=EDGE_LOOP ( 'NONE', ( #5617, #8935, #2202, #9522 ) ) ;
#3383=DIRECTION ( 'NONE',  ( 1.000000000000000000, 0.000000000000000000, 0.000000000000000000 ) ) ;
#3400=EDGE_CURVE ( 'NONE', #11973, #11685, #13232, .T. ) ;
#3427=EDGE_LOOP ( 'NONE', ( #13700, #9566, #11098, #4797 ) ) ;
#3490=LINE ( 'NONE', #8709, #8304 ) ;
#3591=CARTESIAN_POINT ( 'NONE',  ( 134.9999999999999432, -56.99999999999997158, 10.00000000000000178 ) ) ;
#3616=CARTESIAN_POINT ( 'NONE',  ( 124.9999999999999574, -64.99999999999997158, 10.00000000000000000 ) ) ;
#3641=( LENGTH_UNIT ( ) NAMED_UNIT ( * ) SI_UNIT ( .MILLI., .METRE. ) );
#3664=( GEOMETRIC_REPRESENTATION_CONTEXT ( 3 ) GLOBAL_UNCERTAINTY_ASSIGNED_CONTEXT ( ( #3870 ) ) GLOBAL_UNIT_ASSIGNED_CONTEXT ( ( #1848, #11794, #12015 ) ) REPRESENTATION_CONTEXT ( 'NONE', 'WORKASPACE' ) );
#3698=ORIENTED_EDGE ( 'NONE', *, *, #11535, .F. ) ;
#3756=CARTESIAN_POINT ( 'NONE',  ( 144.9999999999999716, -64.99999999999997158, 10.00000000000000000 ) ) ;
#3762=CIRCLE ( 'NONE', #7689, 2.649999999999985700 ) ;
#3773=COLOUR_RGB ( '',0.8941176470588234615, 0.8941176470588234615, 0.8941176470588234615 ) ;
#3870=UNCERTAINTY_MEASURE_WITH_UNIT (LENGTH_MEASURE( 1.000000000000000082E-05 ), #1848, 'distance_accuracy_value', 'NONE');
#3874=APPLICATION_CONTEXT ( 'automotive_design' ) ;
#3938=DIRECTION ( 'NONE',  ( -1.000000000000000000, 0.000000000000000000, 0.000000000000000000 ) ) ;
#3942=CIRCLE ( 'NONE', #10186, 2.649999999999985700 ) ;
#3956=ORIENTED_EDGE ( 'NONE', *, *, #12842, .F. ) ;
#3993=VERTEX_POINT ( 'NONE', #11038 ) ;
#4002=( LENGTH_UNIT ( ) NAMED_UNIT ( * ) SI_UNIT ( .MILLI., .METRE. ) );
#4014=ORIENTED_EDGE ( 'NONE', *, *, #13714, .F. ) ;
#4071=FILL_AREA_STYLE_COLOUR ( '', #3773 ) ;
#4097=EDGE_CURVE ( 'NONE', #5874, #12188, #3490, .T. ) ;
#4100=ORIENTED_EDGE ( 'NONE', *, *, #2150, .F. ) ;
#4138=VERTEX_POINT ( 'NONE', #5799 ) ;
#4205=VERTEX_POINT ( 'NONE', #1436 ) ;
#4208=VERTEX_POINT ( 'NONE', #4863 ) ;
#4235=EDGE_LOOP ( 'NONE', ( #9633, #6493 ) ) ;
#4286=VECTOR ( 'NONE', #10463, 1000.000000000000000 ) ;
#4381=CARTESIAN_POINT ( 'NONE',  ( 137.6499999999999488, -36.99999999999997868, 0.000000000000000000 ) ) ;
#4390=ORIENTED_EDGE ( 'NONE', *, *, #9123, .T. ) ;
#4403=DIRECTION ( 'NONE',  ( -0.000000000000000000, -0.000000000000000000, 1.000000000000000000 ) ) ;
#4418=FACE_OUTER_BOUND ( 'NONE', #3427, .T. ) ;
#4452=DIRECTION ( 'NONE',  ( 0.000000000000000000, -1.000000000000000000, 0.000000000000000000 ) ) ;
#4460=ORIENTED_EDGE ( 'NONE', *, *, #9569, .F. ) ;
#4473=ADVANCED_FACE ( 'NONE', ( #4418 ), #14195, .T. ) ;
#4475=FACE_BOUND ( 'NONE', #6477, .T. ) ;
#4488=CARTESIAN_POINT ( 'NONE',  ( 134.9999999999999716, 45.00000000000001421, 0.000000000000000000 ) ) ;
#4490=LINE ( 'NONE', #5641, #14115 ) ;
#4522=EDGE_CURVE ( 'NONE', #13461, #12188, #4490, .T. ) ;
#4536=CYLINDRICAL_SURFACE ( 'NONE', #8049, 2.649999999999985700 ) ;
#4537=DIRECTION ( 'NONE',  ( 0.000000000000000000, 0.000000000000000000, -1.000000000000000000 ) ) ;
#4676=AXIS2_PLACEMENT_3D ( 'NONE', #10113, #4537, #2359 ) ;
#4721=CYLINDRICAL_SURFACE ( 'NONE', #5948, 2.649999999999985700 ) ;
#4724=EDGE_LOOP ( 'NONE', ( #6818, #12742, #12362, #6874 ) ) ;
#4751=CARTESIAN_POINT ( 'NONE',  ( 144.9999999999999716, -64.99999999999997158, 10.00000000000000000 ) ) ;
#4797=ORIENTED_EDGE ( 'NONE', *, *, #9370, .T. ) ;
#4805=EDGE_CURVE ( 'NONE', #12113, #5384, #13891, .T. ) ;
#4851=PRODUCT_DEFINITION_SHAPE ( 'NONE', 'NONE',  #12238 ) ;
#4863=CARTESIAN_POINT ( 'NONE',  ( 132.3499999999999943, 45.00000000000001421, -1.230770033143087371E-15 ) ) ;
#4923=CARTESIAN_POINT ( 'NONE',  ( 134.9999999999999716, 45.00000000000001421, 10.00000000000000000 ) ) ;
#5015=ORIENTED_EDGE ( 'NONE', *, *, #2292, .F. ) ;
#5021=DIRECTION ( 'NONE',  ( -1.000000000000000000, 0.000000000000000000, 0.000000000000000000 ) ) ;
#5077=DIRECTION ( 'NONE',  ( 1.000000000000000000, 0.000000000000000000, 0.000000000000000000 ) ) ;
#5105=SHAPE_DEFINITION_REPRESENTATION ( #4851, #10713 ) ;
#5108=AXIS2_PLACEMENT_3D ( 'NONE', #5984, #6994, #2362 ) ;
#5110=CARTESIAN_POINT ( 'NONE',  ( 137.6499999999999773, 45.00000000000001421, 0.000000000000000000 ) ) ;
#5115=ORIENTED_EDGE ( 'NONE', *, *, #2196, .F. ) ;
#5117=ORIENTED_EDGE ( 'NONE', *, *, #1413, .T. ) ;
#5140=AXIS2_PLACEMENT_3D ( 'NONE', #87, #10058, #13314 ) ;
#5141=DIRECTION ( 'NONE',  ( -1.000000000000000000, 0.000000000000000000, 0.000000000000000000 ) ) ;
#5142=ORIENTED_EDGE ( 'NONE', *, *, #9370, .F. ) ;
#5179=EDGE_CURVE ( 'NONE', #4205, #1111, #9023, .T. ) ;
#5211=ORIENTED_EDGE ( 'NONE', *, *, #9330, .T. ) ;
#5212=ORIENTED_EDGE ( 'NONE', *, *, #9123, .F. ) ;
#5231=CARTESIAN_POINT ( 'NONE',  ( 134.9999999999999432, -56.99999999999997158, 10.00000000000000178 ) ) ;
#5233=DIRECTION ( 'NONE',  ( -1.000000000000000000, 2.312964634635743450E-16, 0.000000000000000000 ) ) ;
#5238=SURFACE_STYLE_FILL_AREA ( #11837 ) ;
#5292=LINE ( 'NONE', #7301, #9288 ) ;
#5333=EDGE_LOOP ( 'NONE', ( #7625, #9298 ) ) ;
#5344=AXIS2_PLACEMENT_3D ( 'NONE', #1929, #13893, #1857 ) ;
#5380=VECTOR ( 'NONE', #5834, 1000.000000000000000 ) ;
#5384=VERTEX_POINT ( 'NONE', #14233 ) ;
#5496=DIRECTION ( 'NONE',  ( 2.312964634635743450E-16, 1.000000000000000000, 0.000000000000000000 ) ) ;
#5501=AXIS2_PLACEMENT_3D ( 'NONE', #2404, #12342, #2547 ) ;
#5545=CARTESIAN_POINT ( 'NONE',  ( 132.3499999999999659, -36.99999999999997868, 10.00000000000000000 ) ) ;
#5617=ORIENTED_EDGE ( 'NONE', *, *, #64, .F. ) ;
#5641=CARTESIAN_POINT ( 'NONE',  ( 144.9999999999999716, -64.99999999999997158, 10.00000000000000000 ) ) ;
#5689=CARTESIAN_POINT ( 'NONE',  ( 0.000000000000000000, 0.000000000000000000, 10.00000000000000000 ) ) ;
#5712=CIRCLE ( 'NONE', #5501, 2.649999999999985700 ) ;
#5750=ORIENTED_EDGE ( 'NONE', *, *, #10671, .F. ) ;
#5756=CARTESIAN_POINT ( 'NONE',  ( 134.9999999999999432, -56.99999999999997158, 10.00000000000000000 ) ) ;
#5763=LINE ( 'NONE', #7860, #8691 ) ;
#5799=CARTESIAN_POINT ( 'NONE',  ( 132.3499999999999659, -56.99999999999997158, 0.000000000000000000 ) ) ;
#5802=ORIENTED_EDGE ( 'NONE', *, *, #9569, .T. ) ;
#5834=DIRECTION ( 'NONE',  ( -0.000000000000000000, -0.000000000000000000, 1.000000000000000000 ) ) ;
#5874=VERTEX_POINT ( 'NONE', #7686 ) ;
#5885=EDGE_LOOP ( 'NONE', ( #2333, #5142, #10233, #4390 ) ) ;
#5903=CLOSED_SHELL ( 'NONE', ( #2427, #13748, #7827, #2398, #886, #4473, #7300, #8174, #9260, #2774, #13287, #6379 ) ) ;
#5948=AXIS2_PLACEMENT_3D ( 'NONE', #316, #9131, #11317 ) ;
#5953=AXIS2_PLACEMENT_3D ( 'NONE', #8583, #4452, #7559 ) ;
#5984=CARTESIAN_POINT ( 'NONE',  ( 134.9999999999999432, -36.99999999999997868, 10.00000000000000178 ) ) ;
#6010=FACE_OUTER_BOUND ( 'NONE', #1634, .T. ) ;
#6055=ORIENTED_EDGE ( 'NONE', *, *, #8992, .F. ) ;
#6165=DIRECTION ( 'NONE',  ( -0.000000000000000000, -0.000000000000000000, 1.000000000000000000 ) ) ;
#6191=CARTESIAN_POINT ( 'NONE',  ( 137.6499999999999773, 45.00000000000001421, -1.230770033143087371E-15 ) ) ;
#6211=CARTESIAN_POINT ( 'NONE',  ( 144.9999999999999716, -64.99999999999997158, 0.000000000000000000 ) ) ;
#6213=CARTESIAN_POINT ( 'NONE',  ( 134.9999999999999716, 45.00000000000001421, -1.230770033143087371E-15 ) ) ;
#6280=VECTOR ( 'NONE', #4403, 1000.000000000000000 ) ;
#6293=UNCERTAINTY_MEASURE_WITH_UNIT (LENGTH_MEASURE( 1.000000000000000082E-05 ), #4002, 'distance_accuracy_value', 'NONE');
#6312=FACE_OUTER_BOUND ( 'NONE', #9191, .T. ) ;
#6321=PRESENTATION_STYLE_ASSIGNMENT (( #1817 ) ) ;
#6346=LINE ( 'NONE', #1919, #9190 ) ;
#6350=ORIENTED_EDGE ( 'NONE', *, *, #1413, .F. ) ;
#6362=ORIENTED_EDGE ( 'NONE', *, *, #3400, .F. ) ;
#6379=ADVANCED_FACE ( 'NONE', ( #6010 ), #4721, .F. ) ;
#6391=FACE_OUTER_BOUND ( 'NONE', #3361, .T. ) ;
#6401=DIRECTION ( 'NONE',  ( -1.000000000000000000, 0.000000000000000000, 0.000000000000000000 ) ) ;
#6442=AXIS2_PLACEMENT_3D ( 'NONE', #5231, #6165, #3058 ) ;
#6477=EDGE_LOOP ( 'NONE', ( #4100, #6350 ) ) ;
#6493=ORIENTED_EDGE ( 'NONE', *, *, #2881, .T. ) ;
#6503=DIRECTION ( 'NONE',  ( -1.000000000000000000, 0.000000000000000000, 0.000000000000000000 ) ) ;
#6554=CYLINDRICAL_SURFACE ( 'NONE', #14060, 2.649999999999985700 ) ;
#6584=DIRECTION ( 'NONE',  ( -1.000000000000000000, 0.000000000000000000, 0.000000000000000000 ) ) ;
#6601=VECTOR ( 'NONE', #3938, 1000.000000000000000 ) ;
#6709=EDGE_LOOP ( 'NONE', ( #8146, #10815, #3057, #13297 ) ) ;
#6791=DIRECTION ( 'NONE',  ( 1.000000000000000000, 0.000000000000000000, 0.000000000000000000 ) ) ;
#6818=ORIENTED_EDGE ( 'NONE', *, *, #4805, .F. ) ;
#6820=VERTEX_POINT ( 'NONE', #4381 ) ;
#6869=ORIENTED_EDGE ( 'NONE', *, *, #64, .T. ) ;
#6874=ORIENTED_EDGE ( 'NONE', *, *, #2360, .T. ) ;
#6923=FACE_BOUND ( 'NONE', #4235, .T. ) ;
#6959=EDGE_LOOP ( 'NONE', ( #6362, #3956 ) ) ;
#6994=DIRECTION ( 'NONE',  ( -0.000000000000000000, -0.000000000000000000, 1.000000000000000000 ) ) ;
#6996=FACE_OUTER_BOUND ( 'NONE', #6709, .T. ) ;
#7114=PRODUCT_DEFINITION_CONTEXT ( 'detailed design', #3874, 'design' ) ;
#7124=EDGE_CURVE ( 'NONE', #5874, #3993, #8410, .T. ) ;
#7182=DIRECTION ( 'NONE',  ( -1.000000000000000000, 0.000000000000000000, 0.000000000000000000 ) ) ;
#7188=VERTEX_POINT ( 'NONE', #7534 ) ;
#7224=DIRECTION ( 'NONE',  ( 2.312964634635743450E-16, 1.000000000000000000, 0.000000000000000000 ) ) ;
#7233=DIRECTION ( 'NONE',  ( -1.000000000000000000, 0.000000000000000000, 0.000000000000000000 ) ) ;
#7248=ORIENTED_EDGE ( 'NONE', *, *, #12694, .T. ) ;
#7299=DIRECTION ( 'NONE',  ( -2.312964634635743450E-16, -1.000000000000000000, 0.000000000000000000 ) ) ;
#7300=ADVANCED_FACE ( 'NONE', ( #6312 ), #11829, .T. ) ;
#7301=CARTESIAN_POINT ( 'NONE',  ( 124.9999999999999574, -64.99999999999997158, 10.00000000000000000 ) ) ;
#7328=AXIS2_PLACEMENT_3D ( 'NONE', #4488, #12504, #6584 ) ;
#7370=CIRCLE ( 'NONE', #12938, 2.649999999999985700 ) ;
#7403=ORIENTED_EDGE ( 'NONE', *, *, #11535, .T. ) ;
#7431=ORIENTED_EDGE ( 'NONE', *, *, #11462, .T. ) ;
#7480=STYLED_ITEM ( 'NONE', ( #6321 ), #13031 ) ;
#7496=PLANE ( 'NONE',  #5953 ) ;
#7508=ORIENTED_EDGE ( 'NONE', *, *, #16, .F. ) ;
#7524=AXIS2_PLACEMENT_3D ( 'NONE', #1542, #10056, #79 ) ;
#7534=CARTESIAN_POINT ( 'NONE',  ( 132.3499999999999943, 45.00000000000001421, 10.00000000000000000 ) ) ;
#7559=DIRECTION ( 'NONE',  ( 0.000000000000000000, -0.000000000000000000, -1.000000000000000000 ) ) ;
#7565=EDGE_LOOP ( 'NONE', ( #7403, #11254, #1477, #4014 ) ) ;
#7625=ORIENTED_EDGE ( 'NONE', *, *, #5179, .F. ) ;
#7677=DIRECTION ( 'NONE',  ( -2.312964634635743450E-16, -1.000000000000000000, 0.000000000000000000 ) ) ;
#7686=CARTESIAN_POINT ( 'NONE',  ( 124.9999999999999858, 55.00000000000000711, 10.00000000000000000 ) ) ;
#7689=AXIS2_PLACEMENT_3D ( 'NONE', #13283, #9881, #6401 ) ;
#7702=CARTESIAN_POINT ( 'NONE',  ( 137.6499999999999488, -36.99999999999997868, 10.00000000000000000 ) ) ;
#7703=FACE_OUTER_BOUND ( 'NONE', #2257, .T. ) ;
#7709=VECTOR ( 'NONE', #13296, 1000.000000000000000 ) ;
#7776=LINE ( 'NONE', #5545, #7709 ) ;
#7827=ADVANCED_FACE ( 'NONE', ( #2573 ), #24, .F. ) ;
#7839=PRODUCT ( 'vertical suport', 'vertical suport', '', ( #12701 ) ) ;
#7860=CARTESIAN_POINT ( 'NONE',  ( 124.9999999999999858, 55.00000000000000711, 0.000000000000000000 ) ) ;
#7924=DIRECTION ( 'NONE',  ( -0.000000000000000000, -0.000000000000000000, 1.000000000000000000 ) ) ;
#8044=LINE ( 'NONE', #12404, #3314 ) ;
#8049=AXIS2_PLACEMENT_3D ( 'NONE', #5756, #7924, #3383 ) ;
#8095=PLANE ( 'NONE',  #2545 ) ;
#8146=ORIENTED_EDGE ( 'NONE', *, *, #4522, .T. ) ;
#8150=EDGE_CURVE ( 'NONE', #7188, #4208, #6346, .T. ) ;
#8159=CARTESIAN_POINT ( 'NONE',  ( 144.9999999999999716, -64.99999999999997158, 10.00000000000000000 ) ) ;
#8174=ADVANCED_FACE ( 'NONE', ( #7703 ), #7496, .T. ) ;
#8190=DIRECTION ( 'NONE',  ( -0.000000000000000000, -0.000000000000000000, -1.000000000000000000 ) ) ;
#8213=CIRCLE ( 'NONE', #2906, 2.649999999999985700 ) ;
#8220=CARTESIAN_POINT ( 'NONE',  ( 132.3499999999999659, -56.99999999999997158, 10.00000000000000178 ) ) ;
#8293=MECHANICAL_DESIGN_GEOMETRIC_PRESENTATION_REPRESENTATION('',(#159),#3664);
#8304=VECTOR ( 'NONE', #12330, 1000.000000000000000 ) ;
#8325=VECTOR ( 'NONE', #15, 1000.000000000000000 ) ;
#8410=LINE ( 'NONE', #2550, #1988 ) ;
#8454=DIRECTION ( 'NONE',  ( -0.000000000000000000, -0.000000000000000000, -1.000000000000000000 ) ) ;
#8487=SHAPE_REPRESENTATION_RELATIONSHIP ( 'NONE' , 'NONE' ,  #10713, #13031 ) ;
#8583=CARTESIAN_POINT ( 'NONE',  ( 144.9999999999999716, -64.99999999999997158, 10.00000000000000000 ) ) ;
#8595=CARTESIAN_POINT ( 'NONE',  ( 137.6499999999999488, -56.99999999999997158, 10.00000000000000178 ) ) ;
#8622=VERTEX_POINT ( 'NONE', #3616 ) ;
#8691=VECTOR ( 'NONE', #6791, 1000.000000000000000 ) ;
#8709=CARTESIAN_POINT ( 'NONE',  ( 124.9999999999999858, 55.00000000000000711, 10.00000000000000000 ) ) ;
#8848=UNCERTAINTY_MEASURE_WITH_UNIT (LENGTH_MEASURE( 1.000000000000000082E-05 ), #3641, 'distance_accuracy_value', 'NONE');
#8859=ORIENTED_EDGE ( 'NONE', *, *, #12694, .F. ) ;
#8893=LINE ( 'NONE', #10999, #6280 ) ;
#8909=DIRECTION ( 'NONE',  ( 0.000000000000000000, -0.000000000000000000, 1.000000000000000000 ) ) ;
#8935=ORIENTED_EDGE ( 'NONE', *, *, #11258, .F. ) ;
#8954=FACE_BOUND ( 'NONE', #10210, .T. ) ;
#8973=DIRECTION ( 'NONE',  ( 0.000000000000000000, 1.000000000000000000, 0.000000000000000000 ) ) ;
#8992=EDGE_CURVE ( 'NONE', #10379, #3993, #3261, .T. ) ;
#9023=CIRCLE ( 'NONE', #5108, 2.649999999999985700 ) ;
#9092=ORIENTED_EDGE ( 'NONE', *, *, #2881, .F. ) ;
#9105=DIRECTION ( 'NONE',  ( -1.000000000000000000, 0.000000000000000000, -0.000000000000000000 ) ) ;
#9123=EDGE_CURVE ( 'NONE', #13461, #12113, #10341, .T. ) ;
#9131=DIRECTION ( 'NONE',  ( -0.000000000000000000, -0.000000000000000000, 1.000000000000000000 ) ) ;
#9190=VECTOR ( 'NONE', #9752, 1000.000000000000000 ) ;
#9191=EDGE_LOOP ( 'NONE', ( #6055, #5115, #7431, #1362 ) ) ;
#9253=AXIS2_PLACEMENT_3D ( 'NONE', #1044, #8973, #8909 ) ;
#9260=ADVANCED_FACE ( 'NONE', ( #12222, #8954, #4475, #12296 ), #13372, .T. ) ;
#9288=VECTOR ( 'NONE', #3184, 1000.000000000000000 ) ;
#9298=ORIENTED_EDGE ( 'NONE', *, *, #2537, .F. ) ;
#9324=ORIENTED_EDGE ( 'NONE', *, *, #2196, .T. ) ;
#9330=EDGE_CURVE ( 'NONE', #1971, #11973, #8893, .T. ) ;
#9370=EDGE_CURVE ( 'NONE', #12188, #5384, #13244, .T. ) ;
#9401=DIRECTION ( 'NONE',  ( -0.000000000000000000, -0.000000000000000000, -1.000000000000000000 ) ) ;
#9418=DIRECTION ( 'NONE',  ( 0.000000000000000000, 0.000000000000000000, 1.000000000000000000 ) ) ;
#9522=ORIENTED_EDGE ( 'NONE', *, *, #2150, .T. ) ;
#9561=CARTESIAN_POINT ( 'NONE',  ( 132.3499999999999659, -36.99999999999997868, 10.00000000000000178 ) ) ;
#9566=ORIENTED_EDGE ( 'NONE', *, *, #7124, .F. ) ;
#9569=EDGE_CURVE ( 'NONE', #4138, #11685, #10185, .T. ) ;
#9633=ORIENTED_EDGE ( 'NONE', *, *, #11258, .T. ) ;
#9734=CYLINDRICAL_SURFACE ( 'NONE', #14187, 2.649999999999985700 ) ;
#9752=DIRECTION ( 'NONE',  ( -0.000000000000000000, -0.000000000000000000, -1.000000000000000000 ) ) ;
#9772=LINE ( 'NONE', #11145, #8325 ) ;
#9828=EDGE_LOOP ( 'NONE', ( #9092, #6869, #5117, #12012 ) ) ;
#9881=DIRECTION ( 'NONE',  ( -0.000000000000000000, -0.000000000000000000, -1.000000000000000000 ) ) ;
#9956=VECTOR ( 'NONE', #7224, 1000.000000000000000 ) ;
#9984=CARTESIAN_POINT ( 'NONE',  ( 132.3499999999999659, -36.99999999999997868, 0.000000000000000000 ) ) ;
#10056=DIRECTION ( 'NONE',  ( -0.000000000000000000, -0.000000000000000000, 1.000000000000000000 ) ) ;
#10058=DIRECTION ( 'NONE',  ( 0.000000000000000000, 0.000000000000000000, -1.000000000000000000 ) ) ;
#10113=CARTESIAN_POINT ( 'NONE',  ( 0.000000000000000000, 0.000000000000000000, 0.000000000000000000 ) ) ;
#10185=LINE ( 'NONE', #1394, #5380 ) ;
#10186=AXIS2_PLACEMENT_3D ( 'NONE', #6213, #8454, #5141 ) ;
#10188=DIRECTION ( 'NONE',  ( -0.000000000000000000, -0.000000000000000000, 1.000000000000000000 ) ) ;
#10190=FACE_OUTER_BOUND ( 'NONE', #7565, .T. ) ;
#10210=EDGE_LOOP ( 'NONE', ( #5015, #8859 ) ) ;
#10233=ORIENTED_EDGE ( 'NONE', *, *, #4522, .F. ) ;
#10270=ORIENTED_EDGE ( 'NONE', *, *, #2065, .F. ) ;
#10280=DIRECTION ( 'NONE',  ( 0.000000000000000000, 0.000000000000000000, -1.000000000000000000 ) ) ;
#10341=LINE ( 'NONE', #8159, #11154 ) ;
#10379=VERTEX_POINT ( 'NONE', #13086 ) ;
#10463=DIRECTION ( 'NONE',  ( -0.000000000000000000, -0.000000000000000000, -1.000000000000000000 ) ) ;
#10494=PRODUCT_DEFINITION_FORMATION_WITH_SPECIFIED_SOURCE ( 'ANY', '', #7839, .NOT_KNOWN. ) ;
#10508=CARTESIAN_POINT ( 'NONE',  ( 0.000000000000000000, 0.000000000000000000, 0.000000000000000000 ) ) ;
#10637=CIRCLE ( 'NONE', #13863, 2.649999999999985700 ) ;
#10671=EDGE_CURVE ( 'NONE', #3349, #1111, #7776, .T. ) ;
#10713=SHAPE_REPRESENTATION ( 'vertical suport', ( #14039 ), #3056 ) ;
#10752=DIRECTION ( 'NONE',  ( -0.000000000000000000, -0.000000000000000000, -1.000000000000000000 ) ) ;
#10815=ORIENTED_EDGE ( 'NONE', *, *, #4097, .F. ) ;
#10975=ORIENTED_EDGE ( 'NONE', *, *, #12842, .T. ) ;
#10999=CARTESIAN_POINT ( 'NONE',  ( 137.6499999999999488, -56.99999999999997158, 10.00000000000000000 ) ) ;
#11038=CARTESIAN_POINT ( 'NONE',  ( 124.9999999999999858, 55.00000000000000711, 0.000000000000000000 ) ) ;
#11098=ORIENTED_EDGE ( 'NONE', *, *, #4097, .T. ) ;
#11145=CARTESIAN_POINT ( 'NONE',  ( 124.9999999999999574, -64.99999999999997158, 10.00000000000000000 ) ) ;
#11154=VECTOR ( 'NONE', #9401, 1000.000000000000000 ) ;
#11254=ORIENTED_EDGE ( 'NONE', *, *, #10671, .T. ) ;
#11258=EDGE_CURVE ( 'NONE', #7188, #764, #12318, .T. ) ;
#11282=FACE_BOUND ( 'NONE', #5333, .T. ) ;
#11288=APPLICATION_CONTEXT ( 'automotive_design' ) ;
#11317=DIRECTION ( 'NONE',  ( 1.000000000000000000, 0.000000000000000000, 0.000000000000000000 ) ) ;
#11345=CARTESIAN_POINT ( 'NONE',  ( 145.0000000000000000, 55.00000000000000711, 10.00000000000000000 ) ) ;
#11429=FACE_BOUND ( 'NONE', #6959, .T. ) ;
#11462=EDGE_CURVE ( 'NONE', #8622, #5874, #5292, .T. ) ;
#11535=EDGE_CURVE ( 'NONE', #6820, #3349, #12303, .T. ) ;
#11583=CIRCLE ( 'NONE', #5344, 2.649999999999985700 ) ;
#11615=CARTESIAN_POINT ( 'NONE',  ( 134.9999999999999716, 45.00000000000001421, 10.00000000000000000 ) ) ;
#11616=( NAMED_UNIT ( * ) PLANE_ANGLE_UNIT ( ) SI_UNIT ( $, .RADIAN. ) );
#11685=VERTEX_POINT ( 'NONE', #8220 ) ;
#11766=CARTESIAN_POINT ( 'NONE',  ( 134.9999999999999716, 45.00000000000001421, 0.000000000000000000 ) ) ;
#11794=( NAMED_UNIT ( * ) PLANE_ANGLE_UNIT ( ) SI_UNIT ( $, .RADIAN. ) );
#11829=PLANE ( 'NONE',  #2698 ) ;
#11837=FILL_AREA_STYLE ('',( #4071 ) ) ;
#11900=CARTESIAN_POINT ( 'NONE',  ( 137.6499999999999488, -56.99999999999997158, 0.000000000000000000 ) ) ;
#11973=VERTEX_POINT ( 'NONE', #8595 ) ;
#11979=( NAMED_UNIT ( * ) SI_UNIT ( $, .STERADIAN. ) SOLID_ANGLE_UNIT ( ) );
#12012=ORIENTED_EDGE ( 'NONE', *, *, #8150, .F. ) ;
#12015=( NAMED_UNIT ( * ) SI_UNIT ( $, .STERADIAN. ) SOLID_ANGLE_UNIT ( ) );
#12072=DIRECTION ( 'NONE',  ( 1.000000000000000000, 0.000000000000000000, 0.000000000000000000 ) ) ;
#12099=CARTESIAN_POINT ( 'NONE',  ( 124.9999999999999574, -64.99999999999997158, 0.000000000000000000 ) ) ;
#12113=VERTEX_POINT ( 'NONE', #13438 ) ;
#12188=VERTEX_POINT ( 'NONE', #11345 ) ;
#12222=FACE_BOUND ( 'NONE', #12595, .T. ) ;
#12238=PRODUCT_DEFINITION ( 'UNKNOWN', '', #10494, #7114 ) ;
#12269=DIRECTION ( 'NONE',  ( -1.000000000000000000, 0.000000000000000000, 0.000000000000000000 ) ) ;
#12296=FACE_OUTER_BOUND ( 'NONE', #4724, .T. ) ;
#12303=CIRCLE ( 'NONE', #5140, 2.649999999999985700 ) ;
#12318=CIRCLE ( 'NONE', #909, 2.649999999999985700 ) ;
#12330=DIRECTION ( 'NONE',  ( 1.000000000000000000, 0.000000000000000000, 0.000000000000000000 ) ) ;
#12342=DIRECTION ( 'NONE',  ( 0.000000000000000000, 0.000000000000000000, -1.000000000000000000 ) ) ;
#12346=LINE ( 'NONE', #7702, #13148 ) ;
#12347=MECHANICAL_DESIGN_GEOMETRIC_PRESENTATION_REPRESENTATION('',(#7480),#3097);
#12362=ORIENTED_EDGE ( 'NONE', *, *, #8992, .T. ) ;
#12390=AXIS2_PLACEMENT_3D ( 'NONE', #5689, #1256, #9105 ) ;
#12404=CARTESIAN_POINT ( 'NONE',  ( 144.9999999999999716, -64.99999999999997158, 10.00000000000000000 ) ) ;
#12504=DIRECTION ( 'NONE',  ( -0.000000000000000000, -0.000000000000000000, -1.000000000000000000 ) ) ;
#12595=EDGE_LOOP ( 'NONE', ( #3698, #10270 ) ) ;
#12694=EDGE_CURVE ( 'NONE', #4138, #1971, #5712, .T. ) ;
#12701=PRODUCT_CONTEXT ( 'NONE', #11288, 'mechanical' ) ;
#12742=ORIENTED_EDGE ( 'NONE', *, *, #16, .T. ) ;
#12774=DIRECTION ( 'NONE',  ( 0.000000000000000000, 0.000000000000000000, -1.000000000000000000 ) ) ;
#12775=( NAMED_UNIT ( * ) SI_UNIT ( $, .STERADIAN. ) SOLID_ANGLE_UNIT ( ) );
#12842=EDGE_CURVE ( 'NONE', #11685, #11973, #1551, .T. ) ;
#12849=CARTESIAN_POINT ( 'NONE',  ( 144.9999999999999716, -64.99999999999997158, 0.000000000000000000 ) ) ;
#12938=AXIS2_PLACEMENT_3D ( 'NONE', #11615, #12774, #5021 ) ;
#13000=ORIENTED_EDGE ( 'NONE', *, *, #13714, .T. ) ;
#13031=ADVANCED_BREP_SHAPE_REPRESENTATION ( '', ( #13163, #14039 ), #3056 ) ;
#13060=ORIENTED_EDGE ( 'NONE', *, *, #9330, .F. ) ;
#13084=EDGE_LOOP ( 'NONE', ( #4460, #7248, #5211, #2091 ) ) ;
#13086=CARTESIAN_POINT ( 'NONE',  ( 124.9999999999999574, -64.99999999999997158, 0.000000000000000000 ) ) ;
#13148=VECTOR ( 'NONE', #13149, 1000.000000000000000 ) ;
#13149=DIRECTION ( 'NONE',  ( -0.000000000000000000, -0.000000000000000000, 1.000000000000000000 ) ) ;
#13163=MANIFOLD_SOLID_BREP ( 'LPattern1', #5903 ) ;
#13169=CARTESIAN_POINT ( 'NONE',  ( 145.0000000000000000, 55.00000000000000711, 10.00000000000000000 ) ) ;
#13222=DIRECTION ( 'NONE',  ( 1.000000000000000000, 0.000000000000000000, 0.000000000000000000 ) ) ;
#13232=CIRCLE ( 'NONE', #270, 2.649999999999985700 ) ;
#13244=LINE ( 'NONE', #13169, #13927 ) ;
#13283=CARTESIAN_POINT ( 'NONE',  ( 134.9999999999999716, 45.00000000000001421, -1.230770033143087371E-15 ) ) ;
#13287=ADVANCED_FACE ( 'NONE', ( #1324 ), #4536, .F. ) ;
#13296=DIRECTION ( 'NONE',  ( -0.000000000000000000, -0.000000000000000000, 1.000000000000000000 ) ) ;
#13297=ORIENTED_EDGE ( 'NONE', *, *, #1613, .F. ) ;
#13308=CARTESIAN_POINT ( 'NONE',  ( 134.9999999999999432, -56.99999999999997158, 0.000000000000000000 ) ) ;
#13314=DIRECTION ( 'NONE',  ( -1.000000000000000000, 0.000000000000000000, 0.000000000000000000 ) ) ;
#13355=DIRECTION ( 'NONE',  ( -0.000000000000000000, -0.000000000000000000, 1.000000000000000000 ) ) ;
#13372=PLANE ( 'NONE',  #4676 ) ;
#13438=CARTESIAN_POINT ( 'NONE',  ( 144.9999999999999716, -64.99999999999997158, 0.000000000000000000 ) ) ;
#13461=VERTEX_POINT ( 'NONE', #4751 ) ;
#13509=VERTEX_POINT ( 'NONE', #6191 ) ;
#13700=ORIENTED_EDGE ( 'NONE', *, *, #2360, .F. ) ;
#13714=EDGE_CURVE ( 'NONE', #6820, #4205, #12346, .T. ) ;
#13748=ADVANCED_FACE ( 'NONE', ( #14304 ), #6554, .F. ) ;
#13863=AXIS2_PLACEMENT_3D ( 'NONE', #2128, #13355, #12072 ) ;
#13864=LINE ( 'NONE', #12849, #6601 ) ;
#13891=LINE ( 'NONE', #6211, #9956 ) ;
#13893=DIRECTION ( 'NONE',  ( 0.000000000000000000, 0.000000000000000000, -1.000000000000000000 ) ) ;
#13927=VECTOR ( 'NONE', #3248, 1000.000000000000000 ) ;
#14039=AXIS2_PLACEMENT_3D ( 'NONE', #10508, #9418, #5077 ) ;
#14060=AXIS2_PLACEMENT_3D ( 'NONE', #2341, #2147, #13222 ) ;
#14109=DIRECTION ( 'NONE',  ( 0.000000000000000000, 0.000000000000000000, -1.000000000000000000 ) ) ;
#14115=VECTOR ( 'NONE', #5496, 1000.000000000000000 ) ;
#14141=SURFACE_SIDE_STYLE ('',( #5238 ) ) ;
#14187=AXIS2_PLACEMENT_3D ( 'NONE', #11766, #10752, #7182 ) ;
#14195=PLANE ( 'NONE',  #9253 ) ;
#14233=CARTESIAN_POINT ( 'NONE',  ( 145.0000000000000000, 55.00000000000000711, 0.000000000000000000 ) ) ;
#14304=FACE_OUTER_BOUND ( 'NONE', #752, .T. ) ;
#14418=COLOUR_RGB('Off White',0.89,0.88,0.83);
#14419=FILL_AREA_STYLE_COLOUR('',#14418);
#14420=FILL_AREA_STYLE('',(#14419));
#14421=SURFACE_STYLE_FILL_AREA(#14420);
#14422=SURFACE_SIDE_STYLE('',(#14421));
#14423=SURFACE_STYLE_USAGE(.BOTH.,#14422);
#14424=PRESENTATION_STYLE_ASSIGNMENT((#14423));
ENDSEC;
END-ISO-10303-21;
